ISO-10303-21;
HEADER;
/* Generated by software containing ST-Developer
 * from STEP Tools, Inc. (www.steptools.com) 
 */

FILE_DESCRIPTION(
/* description */ ('PAT-054'),
/* implementation_level */ '2;1');

FILE_NAME(
/* name */ 'Cap Screw - M4x16.step',
/* time_stamp */ '2026-10-29T16:38:13-07:00',
/* author */ (''),
/* organization */ (''),
/* preprocessor_version */ 'ST-DEVELOPER v20.2',
/* originating_system */ 'Autodesk Translation Framework v15.17.0.0',
/* authorisation */ '');

FILE_SCHEMA (('AUTOMOTIVE_DESIGN { 1 0 10303 214 3 1 1 }'));
ENDSEC;

DATA;
#10=MECHANICAL_DESIGN_GEOMETRIC_PRESENTATION_REPRESENTATION('',(#946),#33981);
#17=ORIENTED_CLOSED_SHELL('',*,#13060,.F.);
#22=BREP_WITH_VOIDS('Body1',#13059,(#17));
#793=CONICAL_SURFACE('',#14476,0.325,0.785398163397448);
#794=CONICAL_SURFACE('',#14480,0.335,0.785398163397448);
#795=CONICAL_SURFACE('',#14484,0.21,0.463647609000806);
#796=CONICAL_SURFACE('',#14488,0.18,0.785398163397448);
#843=SHAPE_REPRESENTATION_RELATIONSHIP('SRR','None',#34220,#887);
#887=ADVANCED_BREP_SHAPE_REPRESENTATION('',(#22),#33968);
#946=STYLED_ITEM('',(#34524),#22);
#1202=FACE_BOUND('',#2964,.T.);
#1493=PLANE('',#14474);
#1494=PLANE('',#14482);
#1495=PLANE('',#14490);
#1496=PLANE('',#14491);
#1497=PLANE('',#14492);
#1498=PLANE('',#14493);
#1499=PLANE('',#14494);
#1500=PLANE('',#14495);
#1501=PLANE('',#14496);
#1502=PLANE('',#14497);
#1503=PLANE('',#14498);
#2046=FACE_OUTER_BOUND('',#2959,.T.);
#2047=FACE_OUTER_BOUND('',#2960,.T.);
#2048=FACE_OUTER_BOUND('',#2961,.T.);
#2049=FACE_OUTER_BOUND('',#2962,.T.);
#2050=FACE_OUTER_BOUND('',#2963,.T.);
#2051=FACE_OUTER_BOUND('',#2965,.T.);
#2052=FACE_OUTER_BOUND('',#2966,.T.);
#2053=FACE_OUTER_BOUND('',#2967,.T.);
#2054=FACE_OUTER_BOUND('',#2968,.T.);
#2055=FACE_OUTER_BOUND('',#2969,.T.);
#2056=FACE_OUTER_BOUND('',#2970,.T.);
#2057=FACE_OUTER_BOUND('',#2971,.T.);
#2058=FACE_OUTER_BOUND('',#2972,.T.);
#2059=FACE_OUTER_BOUND('',#2973,.T.);
#2060=FACE_OUTER_BOUND('',#2974,.T.);
#2061=FACE_OUTER_BOUND('',#2975,.T.);
#2062=FACE_OUTER_BOUND('',#2976,.T.);
#2959=EDGE_LOOP('',(#10719));
#2960=EDGE_LOOP('',(#10720,#10721,#10722,#10723));
#2961=EDGE_LOOP('',(#10724,#10725,#10726,#10727));
#2962=EDGE_LOOP('',(#10728,#10729,#10730,#10731));
#2963=EDGE_LOOP('',(#10732));
#2964=EDGE_LOOP('',(#10733));
#2965=EDGE_LOOP('',(#10734,#10735,#10736,#10737));
#2966=EDGE_LOOP('',(#10738,#10739,#10740,#10741));
#2967=EDGE_LOOP('',(#10742,#10743,#10744,#10745));
#2968=EDGE_LOOP('',(#10746));
#2969=EDGE_LOOP('',(#10747,#10748,#10749,#10750));
#2970=EDGE_LOOP('',(#10751,#10752,#10753,#10754));
#2971=EDGE_LOOP('',(#10755,#10756,#10757,#10758));
#2972=EDGE_LOOP('',(#10759,#10760,#10761,#10762));
#2973=EDGE_LOOP('',(#10763,#10764,#10765,#10766));
#2974=EDGE_LOOP('',(#10767,#10768,#10769,#10770));
#2975=EDGE_LOOP('',(#10771,#10772,#10773,#10774,#10775,#10776));
#2976=EDGE_LOOP('',(#10777,#10778,#10779,#10780,#10781,#10782));
#3883=LINE('',#23549,#4817);
#3884=LINE('',#23553,#4818);
#3885=LINE('',#23557,#4819);
#3886=LINE('',#23564,#4820);
#3887=LINE('',#23568,#4821);
#3888=LINE('',#23572,#4822);
#3889=LINE('',#23577,#4823);
#3890=LINE('',#23579,#4824);
#3891=LINE('',#23581,#4825);
#3892=LINE('',#23582,#4826);
#3893=LINE('',#23585,#4827);
#3894=LINE('',#23587,#4828);
#3895=LINE('',#23588,#4829);
#3896=LINE('',#23591,#4830);
#3897=LINE('',#23593,#4831);
#3898=LINE('',#23594,#4832);
#3899=LINE('',#23597,#4833);
#3900=LINE('',#23599,#4834);
#3901=LINE('',#23600,#4835);
#3902=LINE('',#23603,#4836);
#3903=LINE('',#23605,#4837);
#3904=LINE('',#23606,#4838);
#3905=LINE('',#23608,#4839);
#3906=LINE('',#23609,#4840);
#4817=VECTOR('',#17374,0.325);
#4818=VECTOR('',#17379,0.35);
#4819=VECTOR('',#17384,0.335);
#4820=VECTOR('',#17393,0.21);
#4821=VECTOR('',#17398,0.2);
#4822=VECTOR('',#17403,0.18);
#4823=VECTOR('',#17408,1.);
#4824=VECTOR('',#17409,1.);
#4825=VECTOR('',#17410,1.);
#4826=VECTOR('',#17411,1.);
#4827=VECTOR('',#17414,1.);
#4828=VECTOR('',#17415,1.);
#4829=VECTOR('',#17416,1.);
#4830=VECTOR('',#17419,1.);
#4831=VECTOR('',#17420,1.);
#4832=VECTOR('',#17421,1.);
#4833=VECTOR('',#17424,1.);
#4834=VECTOR('',#17425,1.);
#4835=VECTOR('',#17426,1.);
#4836=VECTOR('',#17429,1.);
#4837=VECTOR('',#17430,1.);
#4838=VECTOR('',#17431,1.);
#4839=VECTOR('',#17434,1.);
#4840=VECTOR('',#17435,1.);
#5497=CIRCLE('',#14475,0.3);
#5498=CIRCLE('',#14477,0.35);
#5499=CIRCLE('',#14479,0.35);
#5500=CIRCLE('',#14481,0.32);
#5501=CIRCLE('',#14483,0.22);
#5502=CIRCLE('',#14485,0.1954);
#5503=CIRCLE('',#14487,0.1954);
#5504=CIRCLE('',#14489,0.16);
#6328=VERTEX_POINT('',#23544);
#6329=VERTEX_POINT('',#23547);
#6330=VERTEX_POINT('',#23551);
#6331=VERTEX_POINT('',#23555);
#6332=VERTEX_POINT('',#23559);
#6333=VERTEX_POINT('',#23562);
#6334=VERTEX_POINT('',#23566);
#6335=VERTEX_POINT('',#23570);
#6336=VERTEX_POINT('',#23575);
#6337=VERTEX_POINT('',#23576);
#6338=VERTEX_POINT('',#23578);
#6339=VERTEX_POINT('',#23580);
#6340=VERTEX_POINT('',#23584);
#6341=VERTEX_POINT('',#23586);
#6342=VERTEX_POINT('',#23590);
#6343=VERTEX_POINT('',#23592);
#6344=VERTEX_POINT('',#23596);
#6345=VERTEX_POINT('',#23598);
#6346=VERTEX_POINT('',#23602);
#6347=VERTEX_POINT('',#23604);
#7859=EDGE_CURVE('',#6328,#6328,#5497,.T.);
#7860=EDGE_CURVE('',#6329,#6329,#5498,.T.);
#7861=EDGE_CURVE('',#6329,#6328,#3883,.T.);
#7862=EDGE_CURVE('',#6330,#6330,#5499,.T.);
#7863=EDGE_CURVE('',#6330,#6329,#3884,.T.);
#7864=EDGE_CURVE('',#6331,#6331,#5500,.T.);
#7865=EDGE_CURVE('',#6331,#6330,#3885,.T.);
#7866=EDGE_CURVE('',#6332,#6332,#5501,.T.);
#7867=EDGE_CURVE('',#6333,#6333,#5502,.F.);
#7868=EDGE_CURVE('',#6333,#6332,#3886,.T.);
#7869=EDGE_CURVE('',#6334,#6334,#5503,.F.);
#7870=EDGE_CURVE('',#6334,#6333,#3887,.T.);
#7871=EDGE_CURVE('',#6335,#6335,#5504,.T.);
#7872=EDGE_CURVE('',#6335,#6334,#3888,.T.);
#7873=EDGE_CURVE('',#6336,#6337,#3889,.T.);
#7874=EDGE_CURVE('',#6337,#6338,#3890,.T.);
#7875=EDGE_CURVE('',#6338,#6339,#3891,.T.);
#7876=EDGE_CURVE('',#6336,#6339,#3892,.T.);
#7877=EDGE_CURVE('',#6337,#6340,#3893,.T.);
#7878=EDGE_CURVE('',#6340,#6341,#3894,.T.);
#7879=EDGE_CURVE('',#6341,#6338,#3895,.T.);
#7880=EDGE_CURVE('',#6340,#6342,#3896,.T.);
#7881=EDGE_CURVE('',#6342,#6343,#3897,.T.);
#7882=EDGE_CURVE('',#6343,#6341,#3898,.T.);
#7883=EDGE_CURVE('',#6342,#6344,#3899,.T.);
#7884=EDGE_CURVE('',#6344,#6345,#3900,.T.);
#7885=EDGE_CURVE('',#6345,#6343,#3901,.T.);
#7886=EDGE_CURVE('',#6344,#6346,#3902,.T.);
#7887=EDGE_CURVE('',#6346,#6347,#3903,.T.);
#7888=EDGE_CURVE('',#6347,#6345,#3904,.T.);
#7889=EDGE_CURVE('',#6346,#6336,#3905,.T.);
#7890=EDGE_CURVE('',#6339,#6347,#3906,.T.);
#10719=ORIENTED_EDGE('',*,*,#7859,.F.);
#10720=ORIENTED_EDGE('',*,*,#7860,.F.);
#10721=ORIENTED_EDGE('',*,*,#7861,.T.);
#10722=ORIENTED_EDGE('',*,*,#7859,.T.);
#10723=ORIENTED_EDGE('',*,*,#7861,.F.);
#10724=ORIENTED_EDGE('',*,*,#7862,.F.);
#10725=ORIENTED_EDGE('',*,*,#7863,.T.);
#10726=ORIENTED_EDGE('',*,*,#7860,.T.);
#10727=ORIENTED_EDGE('',*,*,#7863,.F.);
#10728=ORIENTED_EDGE('',*,*,#7864,.F.);
#10729=ORIENTED_EDGE('',*,*,#7865,.T.);
#10730=ORIENTED_EDGE('',*,*,#7862,.T.);
#10731=ORIENTED_EDGE('',*,*,#7865,.F.);
#10732=ORIENTED_EDGE('',*,*,#7864,.T.);
#10733=ORIENTED_EDGE('',*,*,#7866,.F.);
#10734=ORIENTED_EDGE('',*,*,#7867,.F.);
#10735=ORIENTED_EDGE('',*,*,#7868,.T.);
#10736=ORIENTED_EDGE('',*,*,#7866,.T.);
#10737=ORIENTED_EDGE('',*,*,#7868,.F.);
#10738=ORIENTED_EDGE('',*,*,#7869,.F.);
#10739=ORIENTED_EDGE('',*,*,#7870,.T.);
#10740=ORIENTED_EDGE('',*,*,#7867,.T.);
#10741=ORIENTED_EDGE('',*,*,#7870,.F.);
#10742=ORIENTED_EDGE('',*,*,#7871,.F.);
#10743=ORIENTED_EDGE('',*,*,#7872,.T.);
#10744=ORIENTED_EDGE('',*,*,#7869,.T.);
#10745=ORIENTED_EDGE('',*,*,#7872,.F.);
#10746=ORIENTED_EDGE('',*,*,#7871,.T.);
#10747=ORIENTED_EDGE('',*,*,#7873,.T.);
#10748=ORIENTED_EDGE('',*,*,#7874,.T.);
#10749=ORIENTED_EDGE('',*,*,#7875,.T.);
#10750=ORIENTED_EDGE('',*,*,#7876,.F.);
#10751=ORIENTED_EDGE('',*,*,#7877,.T.);
#10752=ORIENTED_EDGE('',*,*,#7878,.T.);
#10753=ORIENTED_EDGE('',*,*,#7879,.T.);
#10754=ORIENTED_EDGE('',*,*,#7874,.F.);
#10755=ORIENTED_EDGE('',*,*,#7880,.T.);
#10756=ORIENTED_EDGE('',*,*,#7881,.T.);
#10757=ORIENTED_EDGE('',*,*,#7882,.T.);
#10758=ORIENTED_EDGE('',*,*,#7878,.F.);
#10759=ORIENTED_EDGE('',*,*,#7883,.T.);
#10760=ORIENTED_EDGE('',*,*,#7884,.T.);
#10761=ORIENTED_EDGE('',*,*,#7885,.T.);
#10762=ORIENTED_EDGE('',*,*,#7881,.F.);
#10763=ORIENTED_EDGE('',*,*,#7886,.T.);
#10764=ORIENTED_EDGE('',*,*,#7887,.T.);
#10765=ORIENTED_EDGE('',*,*,#7888,.T.);
#10766=ORIENTED_EDGE('',*,*,#7884,.F.);
#10767=ORIENTED_EDGE('',*,*,#7889,.T.);
#10768=ORIENTED_EDGE('',*,*,#7876,.T.);
#10769=ORIENTED_EDGE('',*,*,#7890,.T.);
#10770=ORIENTED_EDGE('',*,*,#7887,.F.);
#10771=ORIENTED_EDGE('',*,*,#7889,.F.);
#10772=ORIENTED_EDGE('',*,*,#7886,.F.);
#10773=ORIENTED_EDGE('',*,*,#7883,.F.);
#10774=ORIENTED_EDGE('',*,*,#7880,.F.);
#10775=ORIENTED_EDGE('',*,*,#7877,.F.);
#10776=ORIENTED_EDGE('',*,*,#7873,.F.);
#10777=ORIENTED_EDGE('',*,*,#7890,.F.);
#10778=ORIENTED_EDGE('',*,*,#7875,.F.);
#10779=ORIENTED_EDGE('',*,*,#7879,.F.);
#10780=ORIENTED_EDGE('',*,*,#7882,.F.);
#10781=ORIENTED_EDGE('',*,*,#7885,.F.);
#10782=ORIENTED_EDGE('',*,*,#7888,.F.);
#12133=CYLINDRICAL_SURFACE('',#14478,0.35);
#12134=CYLINDRICAL_SURFACE('',#14486,0.1954);
#12758=ADVANCED_FACE('',(#2046),#1493,.T.);
#12759=ADVANCED_FACE('',(#2047),#793,.T.);
#12760=ADVANCED_FACE('',(#2048),#12133,.T.);
#12761=ADVANCED_FACE('',(#2049),#794,.T.);
#12762=ADVANCED_FACE('',(#2050,#1202),#1494,.T.);
#12763=ADVANCED_FACE('',(#2051),#795,.T.);
#12764=ADVANCED_FACE('',(#2052),#12134,.T.);
#12765=ADVANCED_FACE('',(#2053),#796,.T.);
#12766=ADVANCED_FACE('',(#2054),#1495,.T.);
#12767=ADVANCED_FACE('',(#2055),#1496,.F.);
#12768=ADVANCED_FACE('',(#2056),#1497,.F.);
#12769=ADVANCED_FACE('',(#2057),#1498,.F.);
#12770=ADVANCED_FACE('',(#2058),#1499,.F.);
#12771=ADVANCED_FACE('',(#2059),#1500,.F.);
#12772=ADVANCED_FACE('',(#2060),#1501,.F.);
#12773=ADVANCED_FACE('',(#2061),#1502,.F.);
#12774=ADVANCED_FACE('',(#2062),#1503,.F.);
#13059=CLOSED_SHELL('',(#12758,#12759,#12760,#12761,#12762,#12763,#12764,
#12765,#12766));
#13060=CLOSED_SHELL('',(#12767,#12768,#12769,#12770,#12771,#12772,#12773,
#12774));
#14473=AXIS2_PLACEMENT_3D('',#23542,#17364,#17365);
#14474=AXIS2_PLACEMENT_3D('',#23543,#17366,#17367);
#14475=AXIS2_PLACEMENT_3D('',#23545,#17368,#17369);
#14476=AXIS2_PLACEMENT_3D('',#23546,#17370,#17371);
#14477=AXIS2_PLACEMENT_3D('',#23548,#17372,#17373);
#14478=AXIS2_PLACEMENT_3D('',#23550,#17375,#17376);
#14479=AXIS2_PLACEMENT_3D('',#23552,#17377,#17378);
#14480=AXIS2_PLACEMENT_3D('',#23554,#17380,#17381);
#14481=AXIS2_PLACEMENT_3D('',#23556,#17382,#17383);
#14482=AXIS2_PLACEMENT_3D('',#23558,#17385,#17386);
#14483=AXIS2_PLACEMENT_3D('',#23560,#17387,#17388);
#14484=AXIS2_PLACEMENT_3D('',#23561,#17389,#17390);
#14485=AXIS2_PLACEMENT_3D('',#23563,#17391,#17392);
#14486=AXIS2_PLACEMENT_3D('',#23565,#17394,#17395);
#14487=AXIS2_PLACEMENT_3D('',#23567,#17396,#17397);
#14488=AXIS2_PLACEMENT_3D('',#23569,#17399,#17400);
#14489=AXIS2_PLACEMENT_3D('',#23571,#17401,#17402);
#14490=AXIS2_PLACEMENT_3D('',#23573,#17404,#17405);
#14491=AXIS2_PLACEMENT_3D('',#23574,#17406,#17407);
#14492=AXIS2_PLACEMENT_3D('',#23583,#17412,#17413);
#14493=AXIS2_PLACEMENT_3D('',#23589,#17417,#17418);
#14494=AXIS2_PLACEMENT_3D('',#23595,#17422,#17423);
#14495=AXIS2_PLACEMENT_3D('',#23601,#17427,#17428);
#14496=AXIS2_PLACEMENT_3D('',#23607,#17432,#17433);
#14497=AXIS2_PLACEMENT_3D('',#23610,#17436,#17437);
#14498=AXIS2_PLACEMENT_3D('',#23611,#17438,#17439);
#17364=DIRECTION('axis',(0.,0.,1.));
#17365=DIRECTION('refdir',(1.,0.,0.));
#17366=DIRECTION('center_axis',(0.,1.,0.));
#17367=DIRECTION('ref_axis',(0.,0.,1.));
#17368=DIRECTION('center_axis',(0.,-1.,0.));
#17369=DIRECTION('ref_axis',(1.,0.,0.));
#17370=DIRECTION('center_axis',(0.,-1.,0.));
#17371=DIRECTION('ref_axis',(1.,0.,0.));
#17372=DIRECTION('center_axis',(0.,-1.,0.));
#17373=DIRECTION('ref_axis',(1.,0.,0.));
#17374=DIRECTION('',(0.707106781186547,0.707106781186548,8.65956056235493E-17));
#17375=DIRECTION('center_axis',(0.,-1.,0.));
#17376=DIRECTION('ref_axis',(1.,0.,0.));
#17377=DIRECTION('center_axis',(0.,-1.,0.));
#17378=DIRECTION('ref_axis',(1.,0.,0.));
#17379=DIRECTION('',(0.,1.,0.));
#17380=DIRECTION('center_axis',(0.,1.,0.));
#17381=DIRECTION('ref_axis',(1.,0.,0.));
#17382=DIRECTION('center_axis',(0.,-1.,0.));
#17383=DIRECTION('ref_axis',(1.,0.,0.));
#17384=DIRECTION('',(-0.707106781186547,0.707106781186548,-8.65956056235493E-17));
#17385=DIRECTION('center_axis',(0.,-1.,0.));
#17386=DIRECTION('ref_axis',(0.,0.,-1.));
#17387=DIRECTION('center_axis',(0.,-1.,0.));
#17388=DIRECTION('ref_axis',(1.,0.,0.));
#17389=DIRECTION('center_axis',(0.,1.,0.));
#17390=DIRECTION('ref_axis',(1.,0.,0.));
#17391=DIRECTION('center_axis',(0.,1.,0.));
#17392=DIRECTION('ref_axis',(1.,0.,0.));
#17393=DIRECTION('',(-0.447213595499958,0.894427190999916,-5.47678698264203E-17));
#17394=DIRECTION('center_axis',(0.,-1.,0.));
#17395=DIRECTION('ref_axis',(1.,0.,0.));
#17396=DIRECTION('center_axis',(0.,1.,0.));
#17397=DIRECTION('ref_axis',(1.,0.,0.));
#17398=DIRECTION('',(0.,1.,0.));
#17399=DIRECTION('center_axis',(0.,1.,0.));
#17400=DIRECTION('ref_axis',(1.,0.,0.));
#17401=DIRECTION('center_axis',(0.,-1.,0.));
#17402=DIRECTION('ref_axis',(1.,0.,0.));
#17403=DIRECTION('',(-0.707106781186547,0.707106781186548,-8.65956056235493E-17));
#17404=DIRECTION('center_axis',(0.,-1.,0.));
#17405=DIRECTION('ref_axis',(0.,0.,-1.));
#17406=DIRECTION('center_axis',(0.866025403784439,0.,-0.5));
#17407=DIRECTION('ref_axis',(0.5,0.,0.866025403784439));
#17408=DIRECTION('',(-0.5,0.,-0.866025403784439));
#17409=DIRECTION('',(0.,-1.,0.));
#17410=DIRECTION('',(0.5,0.,0.866025403784439));
#17411=DIRECTION('',(0.,-1.,0.));
#17412=DIRECTION('center_axis',(1.60246890531964E-16,0.,-1.));
#17413=DIRECTION('ref_axis',(1.,0.,1.60246890531964E-16));
#17414=DIRECTION('',(-1.,0.,-1.60246890531964E-16));
#17415=DIRECTION('',(0.,-1.,0.));
#17416=DIRECTION('',(1.,0.,1.60246890531964E-16));
#17417=DIRECTION('center_axis',(-0.866025403784439,0.,-0.5));
#17418=DIRECTION('ref_axis',(0.5,0.,-0.866025403784439));
#17419=DIRECTION('',(-0.5,0.,0.866025403784439));
#17420=DIRECTION('',(0.,-1.,0.));
#17421=DIRECTION('',(0.5,0.,-0.866025403784439));
#17422=DIRECTION('center_axis',(-0.866025403784439,0.,0.5));
#17423=DIRECTION('ref_axis',(-0.5,0.,-0.866025403784439));
#17424=DIRECTION('',(0.5,0.,0.866025403784439));
#17425=DIRECTION('',(0.,-1.,0.));
#17426=DIRECTION('',(-0.5,0.,-0.866025403784439));
#17427=DIRECTION('center_axis',(-1.60246890531964E-16,0.,1.));
#17428=DIRECTION('ref_axis',(-1.,0.,-1.60246890531964E-16));
#17429=DIRECTION('',(1.,0.,1.60246890531964E-16));
#17430=DIRECTION('',(0.,-1.,0.));
#17431=DIRECTION('',(-1.,0.,-1.60246890531964E-16));
#17432=DIRECTION('center_axis',(0.866025403784439,0.,0.5));
#17433=DIRECTION('ref_axis',(-0.5,0.,0.866025403784439));
#17434=DIRECTION('',(0.5,0.,-0.866025403784439));
#17435=DIRECTION('',(-0.5,0.,0.866025403784439));
#17436=DIRECTION('center_axis',(0.,1.,0.));
#17437=DIRECTION('ref_axis',(1.,0.,0.));
#17438=DIRECTION('center_axis',(0.,-1.,0.));
#17439=DIRECTION('ref_axis',(0.,0.,-1.));
#23542=CARTESIAN_POINT('',(0.,0.,0.));
#23543=CARTESIAN_POINT('Origin',(0.3,0.4,0.));
#23544=CARTESIAN_POINT('',(-0.3,0.4,-3.67394039744206E-17));
#23545=CARTESIAN_POINT('Origin',(0.,0.4,0.));
#23546=CARTESIAN_POINT('Origin',(0.,0.375,0.));
#23547=CARTESIAN_POINT('',(-0.35,0.35,-4.28626379701573E-17));
#23548=CARTESIAN_POINT('Origin',(0.,0.35,0.));
#23549=CARTESIAN_POINT('',(-0.325,0.375,-3.9801020972289E-17));
#23550=CARTESIAN_POINT('Origin',(0.,0.19,0.));
#23551=CARTESIAN_POINT('',(-0.35,0.03,-4.28626379701574E-17));
#23552=CARTESIAN_POINT('Origin',(0.,0.03,0.));
#23553=CARTESIAN_POINT('',(-0.35,0.19,-4.28626379701574E-17));
#23554=CARTESIAN_POINT('Origin',(0.,0.0149999999999999,0.));
#23555=CARTESIAN_POINT('',(-0.32,-3.29597460435593E-17,-3.91886975727153E-17));
#23556=CARTESIAN_POINT('Origin',(0.,0.,0.));
#23557=CARTESIAN_POINT('',(-0.335,0.0149999999999999,-4.10256677714363E-17));
#23558=CARTESIAN_POINT('Origin',(0.22,0.,0.));
#23559=CARTESIAN_POINT('',(-0.22,-6.93889390390723E-18,-2.69422295812418E-17));
#23560=CARTESIAN_POINT('Origin',(0.,0.,0.));
#23561=CARTESIAN_POINT('Origin',(0.,-0.02,0.));
#23562=CARTESIAN_POINT('',(-0.1954,-0.0492,2.39295984553393E-17));
#23563=CARTESIAN_POINT('Origin',(0.,-0.0492,0.));
#23564=CARTESIAN_POINT('',(-0.21,-0.02,-2.57175827820944E-17));
#23565=CARTESIAN_POINT('Origin',(0.,-0.8,0.));
#23566=CARTESIAN_POINT('',(-0.1954,-1.5646,2.39295984553393E-17));
#23567=CARTESIAN_POINT('Origin',(0.,-1.5646,0.));
#23568=CARTESIAN_POINT('',(-0.1954,-0.8,-2.39295984553393E-17));
#23569=CARTESIAN_POINT('Origin',(0.,-1.58,0.));
#23570=CARTESIAN_POINT('',(-0.16,-1.6,-1.95943487863577E-17));
#23571=CARTESIAN_POINT('Origin',(0.,-1.6,0.));
#23572=CARTESIAN_POINT('',(-0.18,-1.58,-2.20436423846524E-17));
#23573=CARTESIAN_POINT('Origin',(0.,-1.6,0.));
#23574=CARTESIAN_POINT('Origin',(0.0866025403784439,-0.4,-0.15));
#23575=CARTESIAN_POINT('',(0.173205080756888,-0.4,0.));
#23576=CARTESIAN_POINT('',(0.0866025403784439,-0.4,-0.15));
#23577=CARTESIAN_POINT('',(0.173205080756888,-0.4,0.));
#23578=CARTESIAN_POINT('',(0.0866025403784439,-0.64,-0.15));
#23579=CARTESIAN_POINT('',(0.0866025403784439,-0.4,-0.15));
#23580=CARTESIAN_POINT('',(0.173205080756888,-0.64,0.));
#23581=CARTESIAN_POINT('',(0.173205080756888,-0.64,0.));
#23582=CARTESIAN_POINT('',(0.173205080756888,-0.4,0.));
#23583=CARTESIAN_POINT('Origin',(-0.0866025403784438,-0.4,-0.15));
#23584=CARTESIAN_POINT('',(-0.0866025403784438,-0.4,-0.15));
#23585=CARTESIAN_POINT('',(0.0866025403784439,-0.4,-0.15));
#23586=CARTESIAN_POINT('',(-0.0866025403784438,-0.64,-0.15));
#23587=CARTESIAN_POINT('',(-0.0866025403784438,-0.4,-0.15));
#23588=CARTESIAN_POINT('',(0.0866025403784439,-0.64,-0.15));
#23589=CARTESIAN_POINT('Origin',(-0.173205080756888,-0.4,-2.77555756156289E-17));
#23590=CARTESIAN_POINT('',(-0.173205080756888,-0.4,-2.12115047744981E-17));
#23591=CARTESIAN_POINT('',(-0.0866025403784438,-0.4,-0.15));
#23592=CARTESIAN_POINT('',(-0.173205080756888,-0.64,-2.77555756156289E-17));
#23593=CARTESIAN_POINT('',(-0.173205080756888,-0.4,-2.12115047744981E-17));
#23594=CARTESIAN_POINT('',(-0.0866025403784438,-0.64,-0.15));
#23595=CARTESIAN_POINT('Origin',(-0.0866025403784439,-0.4,0.15));
#23596=CARTESIAN_POINT('',(-0.0866025403784439,-0.4,0.15));
#23597=CARTESIAN_POINT('',(-0.173205080756888,-0.4,-2.12115047744981E-17));
#23598=CARTESIAN_POINT('',(-0.0866025403784439,-0.64,0.15));
#23599=CARTESIAN_POINT('',(-0.0866025403784439,-0.4,0.15));
#23600=CARTESIAN_POINT('',(-0.173205080756888,-0.64,-2.12115047744981E-17));
#23601=CARTESIAN_POINT('Origin',(0.0866025403784439,-0.4,0.15));
#23602=CARTESIAN_POINT('',(0.0866025403784439,-0.4,0.15));
#23603=CARTESIAN_POINT('',(-0.0866025403784439,-0.4,0.15));
#23604=CARTESIAN_POINT('',(0.0866025403784439,-0.64,0.15));
#23605=CARTESIAN_POINT('',(0.0866025403784439,-0.4,0.15));
#23606=CARTESIAN_POINT('',(-0.0866025403784439,-0.64,0.15));
#23607=CARTESIAN_POINT('Origin',(0.173205080756888,-0.4,0.));
#23608=CARTESIAN_POINT('',(0.0866025403784439,-0.4,0.15));
#23609=CARTESIAN_POINT('',(0.0866025403784439,-0.64,0.15));
#23610=CARTESIAN_POINT('Origin',(0.,-0.4,-2.77555756156289E-17));
#23611=CARTESIAN_POINT('Origin',(0.,-0.64,-2.77555756156289E-17));
#33916=UNCERTAINTY_MEASURE_WITH_UNIT(LENGTH_MEASURE(0.001),#33982,
'DISTANCE_ACCURACY_VALUE',
'Maximum model space distance between geometric entities at asserted c
onnectivities');
#33929=UNCERTAINTY_MEASURE_WITH_UNIT(LENGTH_MEASURE(0.001),#33982,
'DISTANCE_ACCURACY_VALUE',
'Maximum model space distance between geometric entities at asserted c
onnectivities');
#33968=(
GEOMETRIC_REPRESENTATION_CONTEXT(3)
GLOBAL_UNCERTAINTY_ASSIGNED_CONTEXT((#33916))
GLOBAL_UNIT_ASSIGNED_CONTEXT((#33982,#33984,#33985))
REPRESENTATION_CONTEXT('','3D')
);
#33981=(
GEOMETRIC_REPRESENTATION_CONTEXT(3)
GLOBAL_UNCERTAINTY_ASSIGNED_CONTEXT((#33929))
GLOBAL_UNIT_ASSIGNED_CONTEXT((#33982,#33984,#33985))
REPRESENTATION_CONTEXT('','3D')
);
#33982=(
LENGTH_UNIT()
NAMED_UNIT(*)
SI_UNIT(.CENTI.,.METRE.)
);
#33984=(
NAMED_UNIT(*)
PLANE_ANGLE_UNIT()
SI_UNIT($,.RADIAN.)
);
#33985=(
NAMED_UNIT(*)
SI_UNIT($,.STERADIAN.)
SOLID_ANGLE_UNIT()
);
#34024=SHAPE_DEFINITION_REPRESENTATION(#34088,#34220);
#34088=PRODUCT_DEFINITION_SHAPE('',$,#34272);
#34220=SHAPE_REPRESENTATION('',(#14473),#33968);
#34233=PRODUCT_DEFINITION_CONTEXT('part definition',#34388,'design');
#34272=PRODUCT_DEFINITION('Cap Screw - M4x16','Cap Screw - M4x16',#34323,
#34233);
#34323=PRODUCT_DEFINITION_FORMATION('',$,#34428);
#34388=APPLICATION_CONTEXT(
'Core Data for Automotive Mechanical Design Process');
#34389=PRODUCT_CONTEXT('part definition',#34388,'mechanical');
#34428=PRODUCT('Cap Screw - M4x16','Cap Screw - M4x16',
'Cap Screw - M4x16',(#34389));
#34518=COLOUR_RGB('Black',0.12,0.14,0.17);
#34519=FILL_AREA_STYLE_COLOUR('',#34518);
#34520=FILL_AREA_STYLE('',(#34519));
#34521=SURFACE_STYLE_FILL_AREA(#34520);
#34522=SURFACE_SIDE_STYLE('',(#34521));
#34523=SURFACE_STYLE_USAGE(.BOTH.,#34522);
#34524=PRESENTATION_STYLE_ASSIGNMENT((#34523));
ENDSEC;
END-ISO-10303-21;
